ISO-10303-21;
HEADER;
/* Generated by software containing ST-Developer
 * from STEP Tools, Inc. (www.steptools.com) 
 */

FILE_DESCRIPTION(
/* description */ ('Rotary union on bearing shaft'),
/* implementation_level */ '2;1');

FILE_NAME(
/* name */ 'Cap Screw - M6x25.step',
/* time_stamp */ '2026-10-28T03:24:01-07:00',
/* author */ (''),
/* organization */ (''),
/* preprocessor_version */ 'ST-DEVELOPER v20.2',
/* originating_system */ 'Autodesk Translation Framework v15.17.0.0',
/* authorisation */ '');

FILE_SCHEMA (('AUTOMOTIVE_DESIGN { 1 0 10303 214 3 1 1 }'));
ENDSEC;

DATA;
#10=MECHANICAL_DESIGN_GEOMETRIC_PRESENTATION_REPRESENTATION('',(#337),#9448);
#11=ORIENTED_CLOSED_SHELL('',*,#4893,.F.);
#14=BREP_WITH_VOIDS('Body1',#4892,(#11));
#205=CONICAL_SURFACE('',#5564,0.475,0.785398163397449);
#206=CONICAL_SURFACE('',#5568,0.485,0.785398163397448);
#207=CONICAL_SURFACE('',#5572,0.31,0.463647609000806);
#208=CONICAL_SURFACE('',#5576,0.27,0.785398163397448);
#275=SHAPE_REPRESENTATION_RELATIONSHIP('SRR','None',#9576,#302);
#302=ADVANCED_BREP_SHAPE_REPRESENTATION('',(#14),#9436);
#337=STYLED_ITEM('',(#9785),#14);
#453=FACE_BOUND('',#1195,.T.);
#567=PLANE('',#5562);
#568=PLANE('',#5570);
#569=PLANE('',#5578);
#570=PLANE('',#5579);
#571=PLANE('',#5580);
#572=PLANE('',#5581);
#573=PLANE('',#5582);
#574=PLANE('',#5583);
#575=PLANE('',#5584);
#576=PLANE('',#5585);
#577=PLANE('',#5586);
#818=FACE_OUTER_BOUND('',#1190,.T.);
#819=FACE_OUTER_BOUND('',#1191,.T.);
#820=FACE_OUTER_BOUND('',#1192,.T.);
#821=FACE_OUTER_BOUND('',#1193,.T.);
#822=FACE_OUTER_BOUND('',#1194,.T.);
#823=FACE_OUTER_BOUND('',#1196,.T.);
#824=FACE_OUTER_BOUND('',#1197,.T.);
#825=FACE_OUTER_BOUND('',#1198,.T.);
#826=FACE_OUTER_BOUND('',#1199,.T.);
#827=FACE_OUTER_BOUND('',#1200,.T.);
#828=FACE_OUTER_BOUND('',#1201,.T.);
#829=FACE_OUTER_BOUND('',#1202,.T.);
#830=FACE_OUTER_BOUND('',#1203,.T.);
#831=FACE_OUTER_BOUND('',#1204,.T.);
#832=FACE_OUTER_BOUND('',#1205,.T.);
#833=FACE_OUTER_BOUND('',#1206,.T.);
#834=FACE_OUTER_BOUND('',#1207,.T.);
#1190=EDGE_LOOP('',(#3935));
#1191=EDGE_LOOP('',(#3936,#3937,#3938,#3939));
#1192=EDGE_LOOP('',(#3940,#3941,#3942,#3943));
#1193=EDGE_LOOP('',(#3944,#3945,#3946,#3947));
#1194=EDGE_LOOP('',(#3948));
#1195=EDGE_LOOP('',(#3949));
#1196=EDGE_LOOP('',(#3950,#3951,#3952,#3953));
#1197=EDGE_LOOP('',(#3954,#3955,#3956,#3957));
#1198=EDGE_LOOP('',(#3958,#3959,#3960,#3961));
#1199=EDGE_LOOP('',(#3962));
#1200=EDGE_LOOP('',(#3963,#3964,#3965,#3966));
#1201=EDGE_LOOP('',(#3967,#3968,#3969,#3970));
#1202=EDGE_LOOP('',(#3971,#3972,#3973,#3974));
#1203=EDGE_LOOP('',(#3975,#3976,#3977,#3978));
#1204=EDGE_LOOP('',(#3979,#3980,#3981,#3982));
#1205=EDGE_LOOP('',(#3983,#3984,#3985,#3986));
#1206=EDGE_LOOP('',(#3987,#3988,#3989,#3990,#3991,#3992));
#1207=EDGE_LOOP('',(#3993,#3994,#3995,#3996,#3997,#3998));
#1498=LINE('',#8621,#1818);
#1499=LINE('',#8625,#1819);
#1500=LINE('',#8629,#1820);
#1501=LINE('',#8636,#1821);
#1502=LINE('',#8640,#1822);
#1503=LINE('',#8644,#1823);
#1504=LINE('',#8649,#1824);
#1505=LINE('',#8651,#1825);
#1506=LINE('',#8653,#1826);
#1507=LINE('',#8654,#1827);
#1508=LINE('',#8657,#1828);
#1509=LINE('',#8659,#1829);
#1510=LINE('',#8660,#1830);
#1511=LINE('',#8663,#1831);
#1512=LINE('',#8665,#1832);
#1513=LINE('',#8666,#1833);
#1514=LINE('',#8669,#1834);
#1515=LINE('',#8671,#1835);
#1516=LINE('',#8672,#1836);
#1517=LINE('',#8675,#1837);
#1518=LINE('',#8677,#1838);
#1519=LINE('',#8678,#1839);
#1520=LINE('',#8680,#1840);
#1521=LINE('',#8681,#1841);
#1818=VECTOR('',#6689,0.475);
#1819=VECTOR('',#6694,0.5);
#1820=VECTOR('',#6699,0.485);
#1821=VECTOR('',#6708,0.31);
#1822=VECTOR('',#6713,0.3);
#1823=VECTOR('',#6718,0.27);
#1824=VECTOR('',#6723,1.);
#1825=VECTOR('',#6724,1.);
#1826=VECTOR('',#6725,1.);
#1827=VECTOR('',#6726,1.);
#1828=VECTOR('',#6729,1.);
#1829=VECTOR('',#6730,1.);
#1830=VECTOR('',#6731,1.);
#1831=VECTOR('',#6734,1.);
#1832=VECTOR('',#6735,1.);
#1833=VECTOR('',#6736,1.);
#1834=VECTOR('',#6739,1.);
#1835=VECTOR('',#6740,1.);
#1836=VECTOR('',#6741,1.);
#1837=VECTOR('',#6744,1.);
#1838=VECTOR('',#6745,1.);
#1839=VECTOR('',#6746,1.);
#1840=VECTOR('',#6749,1.);
#1841=VECTOR('',#6750,1.);
#2172=CIRCLE('',#5563,0.45);
#2173=CIRCLE('',#5565,0.5);
#2174=CIRCLE('',#5567,0.5);
#2175=CIRCLE('',#5569,0.47);
#2176=CIRCLE('',#5571,0.32);
#2177=CIRCLE('',#5573,0.2942);
#2178=CIRCLE('',#5575,0.2942);
#2179=CIRCLE('',#5577,0.24);
#2484=VERTEX_POINT('',#8616);
#2485=VERTEX_POINT('',#8619);
#2486=VERTEX_POINT('',#8623);
#2487=VERTEX_POINT('',#8627);
#2488=VERTEX_POINT('',#8631);
#2489=VERTEX_POINT('',#8634);
#2490=VERTEX_POINT('',#8638);
#2491=VERTEX_POINT('',#8642);
#2492=VERTEX_POINT('',#8647);
#2493=VERTEX_POINT('',#8648);
#2494=VERTEX_POINT('',#8650);
#2495=VERTEX_POINT('',#8652);
#2496=VERTEX_POINT('',#8656);
#2497=VERTEX_POINT('',#8658);
#2498=VERTEX_POINT('',#8662);
#2499=VERTEX_POINT('',#8664);
#2500=VERTEX_POINT('',#8668);
#2501=VERTEX_POINT('',#8670);
#2502=VERTEX_POINT('',#8674);
#2503=VERTEX_POINT('',#8676);
#2995=EDGE_CURVE('',#2484,#2484,#2172,.T.);
#2996=EDGE_CURVE('',#2485,#2485,#2173,.T.);
#2997=EDGE_CURVE('',#2485,#2484,#1498,.T.);
#2998=EDGE_CURVE('',#2486,#2486,#2174,.T.);
#2999=EDGE_CURVE('',#2486,#2485,#1499,.T.);
#3000=EDGE_CURVE('',#2487,#2487,#2175,.T.);
#3001=EDGE_CURVE('',#2487,#2486,#1500,.T.);
#3002=EDGE_CURVE('',#2488,#2488,#2176,.T.);
#3003=EDGE_CURVE('',#2489,#2489,#2177,.F.);
#3004=EDGE_CURVE('',#2489,#2488,#1501,.T.);
#3005=EDGE_CURVE('',#2490,#2490,#2178,.F.);
#3006=EDGE_CURVE('',#2490,#2489,#1502,.T.);
#3007=EDGE_CURVE('',#2491,#2491,#2179,.T.);
#3008=EDGE_CURVE('',#2491,#2490,#1503,.T.);
#3009=EDGE_CURVE('',#2492,#2493,#1504,.T.);
#3010=EDGE_CURVE('',#2493,#2494,#1505,.T.);
#3011=EDGE_CURVE('',#2494,#2495,#1506,.T.);
#3012=EDGE_CURVE('',#2492,#2495,#1507,.T.);
#3013=EDGE_CURVE('',#2493,#2496,#1508,.T.);
#3014=EDGE_CURVE('',#2496,#2497,#1509,.T.);
#3015=EDGE_CURVE('',#2497,#2494,#1510,.T.);
#3016=EDGE_CURVE('',#2496,#2498,#1511,.T.);
#3017=EDGE_CURVE('',#2498,#2499,#1512,.T.);
#3018=EDGE_CURVE('',#2499,#2497,#1513,.T.);
#3019=EDGE_CURVE('',#2498,#2500,#1514,.T.);
#3020=EDGE_CURVE('',#2500,#2501,#1515,.T.);
#3021=EDGE_CURVE('',#2501,#2499,#1516,.T.);
#3022=EDGE_CURVE('',#2500,#2502,#1517,.T.);
#3023=EDGE_CURVE('',#2502,#2503,#1518,.T.);
#3024=EDGE_CURVE('',#2503,#2501,#1519,.T.);
#3025=EDGE_CURVE('',#2502,#2492,#1520,.T.);
#3026=EDGE_CURVE('',#2495,#2503,#1521,.T.);
#3935=ORIENTED_EDGE('',*,*,#2995,.F.);
#3936=ORIENTED_EDGE('',*,*,#2996,.F.);
#3937=ORIENTED_EDGE('',*,*,#2997,.T.);
#3938=ORIENTED_EDGE('',*,*,#2995,.T.);
#3939=ORIENTED_EDGE('',*,*,#2997,.F.);
#3940=ORIENTED_EDGE('',*,*,#2998,.F.);
#3941=ORIENTED_EDGE('',*,*,#2999,.T.);
#3942=ORIENTED_EDGE('',*,*,#2996,.T.);
#3943=ORIENTED_EDGE('',*,*,#2999,.F.);
#3944=ORIENTED_EDGE('',*,*,#3000,.F.);
#3945=ORIENTED_EDGE('',*,*,#3001,.T.);
#3946=ORIENTED_EDGE('',*,*,#2998,.T.);
#3947=ORIENTED_EDGE('',*,*,#3001,.F.);
#3948=ORIENTED_EDGE('',*,*,#3000,.T.);
#3949=ORIENTED_EDGE('',*,*,#3002,.F.);
#3950=ORIENTED_EDGE('',*,*,#3003,.F.);
#3951=ORIENTED_EDGE('',*,*,#3004,.T.);
#3952=ORIENTED_EDGE('',*,*,#3002,.T.);
#3953=ORIENTED_EDGE('',*,*,#3004,.F.);
#3954=ORIENTED_EDGE('',*,*,#3005,.F.);
#3955=ORIENTED_EDGE('',*,*,#3006,.T.);
#3956=ORIENTED_EDGE('',*,*,#3003,.T.);
#3957=ORIENTED_EDGE('',*,*,#3006,.F.);
#3958=ORIENTED_EDGE('',*,*,#3007,.F.);
#3959=ORIENTED_EDGE('',*,*,#3008,.T.);
#3960=ORIENTED_EDGE('',*,*,#3005,.T.);
#3961=ORIENTED_EDGE('',*,*,#3008,.F.);
#3962=ORIENTED_EDGE('',*,*,#3007,.T.);
#3963=ORIENTED_EDGE('',*,*,#3009,.T.);
#3964=ORIENTED_EDGE('',*,*,#3010,.T.);
#3965=ORIENTED_EDGE('',*,*,#3011,.T.);
#3966=ORIENTED_EDGE('',*,*,#3012,.F.);
#3967=ORIENTED_EDGE('',*,*,#3013,.T.);
#3968=ORIENTED_EDGE('',*,*,#3014,.T.);
#3969=ORIENTED_EDGE('',*,*,#3015,.T.);
#3970=ORIENTED_EDGE('',*,*,#3010,.F.);
#3971=ORIENTED_EDGE('',*,*,#3016,.T.);
#3972=ORIENTED_EDGE('',*,*,#3017,.T.);
#3973=ORIENTED_EDGE('',*,*,#3018,.T.);
#3974=ORIENTED_EDGE('',*,*,#3014,.F.);
#3975=ORIENTED_EDGE('',*,*,#3019,.T.);
#3976=ORIENTED_EDGE('',*,*,#3020,.T.);
#3977=ORIENTED_EDGE('',*,*,#3021,.T.);
#3978=ORIENTED_EDGE('',*,*,#3017,.F.);
#3979=ORIENTED_EDGE('',*,*,#3022,.T.);
#3980=ORIENTED_EDGE('',*,*,#3023,.T.);
#3981=ORIENTED_EDGE('',*,*,#3024,.T.);
#3982=ORIENTED_EDGE('',*,*,#3020,.F.);
#3983=ORIENTED_EDGE('',*,*,#3025,.T.);
#3984=ORIENTED_EDGE('',*,*,#3012,.T.);
#3985=ORIENTED_EDGE('',*,*,#3026,.T.);
#3986=ORIENTED_EDGE('',*,*,#3023,.F.);
#3987=ORIENTED_EDGE('',*,*,#3025,.F.);
#3988=ORIENTED_EDGE('',*,*,#3022,.F.);
#3989=ORIENTED_EDGE('',*,*,#3019,.F.);
#3990=ORIENTED_EDGE('',*,*,#3016,.F.);
#3991=ORIENTED_EDGE('',*,*,#3013,.F.);
#3992=ORIENTED_EDGE('',*,*,#3009,.F.);
#3993=ORIENTED_EDGE('',*,*,#3026,.F.);
#3994=ORIENTED_EDGE('',*,*,#3011,.F.);
#3995=ORIENTED_EDGE('',*,*,#3015,.F.);
#3996=ORIENTED_EDGE('',*,*,#3018,.F.);
#3997=ORIENTED_EDGE('',*,*,#3021,.F.);
#3998=ORIENTED_EDGE('',*,*,#3024,.F.);
#4537=CYLINDRICAL_SURFACE('',#5566,0.5);
#4538=CYLINDRICAL_SURFACE('',#5574,0.2942);
#4731=ADVANCED_FACE('',(#818),#567,.T.);
#4732=ADVANCED_FACE('',(#819),#205,.T.);
#4733=ADVANCED_FACE('',(#820),#4537,.T.);
#4734=ADVANCED_FACE('',(#821),#206,.T.);
#4735=ADVANCED_FACE('',(#822,#453),#568,.T.);
#4736=ADVANCED_FACE('',(#823),#207,.T.);
#4737=ADVANCED_FACE('',(#824),#4538,.T.);
#4738=ADVANCED_FACE('',(#825),#208,.T.);
#4739=ADVANCED_FACE('',(#826),#569,.T.);
#4740=ADVANCED_FACE('',(#827),#570,.F.);
#4741=ADVANCED_FACE('',(#828),#571,.F.);
#4742=ADVANCED_FACE('',(#829),#572,.F.);
#4743=ADVANCED_FACE('',(#830),#573,.F.);
#4744=ADVANCED_FACE('',(#831),#574,.F.);
#4745=ADVANCED_FACE('',(#832),#575,.F.);
#4746=ADVANCED_FACE('',(#833),#576,.F.);
#4747=ADVANCED_FACE('',(#834),#577,.F.);
#4892=CLOSED_SHELL('',(#4731,#4732,#4733,#4734,#4735,#4736,#4737,#4738,
#4739));
#4893=CLOSED_SHELL('',(#4740,#4741,#4742,#4743,#4744,#4745,#4746,#4747));
#5561=AXIS2_PLACEMENT_3D('',#8614,#6679,#6680);
#5562=AXIS2_PLACEMENT_3D('',#8615,#6681,#6682);
#5563=AXIS2_PLACEMENT_3D('',#8617,#6683,#6684);
#5564=AXIS2_PLACEMENT_3D('',#8618,#6685,#6686);
#5565=AXIS2_PLACEMENT_3D('',#8620,#6687,#6688);
#5566=AXIS2_PLACEMENT_3D('',#8622,#6690,#6691);
#5567=AXIS2_PLACEMENT_3D('',#8624,#6692,#6693);
#5568=AXIS2_PLACEMENT_3D('',#8626,#6695,#6696);
#5569=AXIS2_PLACEMENT_3D('',#8628,#6697,#6698);
#5570=AXIS2_PLACEMENT_3D('',#8630,#6700,#6701);
#5571=AXIS2_PLACEMENT_3D('',#8632,#6702,#6703);
#5572=AXIS2_PLACEMENT_3D('',#8633,#6704,#6705);
#5573=AXIS2_PLACEMENT_3D('',#8635,#6706,#6707);
#5574=AXIS2_PLACEMENT_3D('',#8637,#6709,#6710);
#5575=AXIS2_PLACEMENT_3D('',#8639,#6711,#6712);
#5576=AXIS2_PLACEMENT_3D('',#8641,#6714,#6715);
#5577=AXIS2_PLACEMENT_3D('',#8643,#6716,#6717);
#5578=AXIS2_PLACEMENT_3D('',#8645,#6719,#6720);
#5579=AXIS2_PLACEMENT_3D('',#8646,#6721,#6722);
#5580=AXIS2_PLACEMENT_3D('',#8655,#6727,#6728);
#5581=AXIS2_PLACEMENT_3D('',#8661,#6732,#6733);
#5582=AXIS2_PLACEMENT_3D('',#8667,#6737,#6738);
#5583=AXIS2_PLACEMENT_3D('',#8673,#6742,#6743);
#5584=AXIS2_PLACEMENT_3D('',#8679,#6747,#6748);
#5585=AXIS2_PLACEMENT_3D('',#8682,#6751,#6752);
#5586=AXIS2_PLACEMENT_3D('',#8683,#6753,#6754);
#6679=DIRECTION('axis',(0.,0.,1.));
#6680=DIRECTION('refdir',(1.,0.,0.));
#6681=DIRECTION('center_axis',(0.,1.,0.));
#6682=DIRECTION('ref_axis',(0.,0.,1.));
#6683=DIRECTION('center_axis',(0.,-1.,0.));
#6684=DIRECTION('ref_axis',(1.,0.,0.));
#6685=DIRECTION('center_axis',(0.,-1.,0.));
#6686=DIRECTION('ref_axis',(1.,0.,0.));
#6687=DIRECTION('center_axis',(0.,-1.,0.));
#6688=DIRECTION('ref_axis',(1.,0.,0.));
#6689=DIRECTION('',(0.707106781186548,0.707106781186547,8.65956056235494E-17));
#6690=DIRECTION('center_axis',(0.,-1.,0.));
#6691=DIRECTION('ref_axis',(1.,0.,0.));
#6692=DIRECTION('center_axis',(0.,-1.,0.));
#6693=DIRECTION('ref_axis',(1.,0.,0.));
#6694=DIRECTION('',(0.,1.,0.));
#6695=DIRECTION('center_axis',(0.,1.,0.));
#6696=DIRECTION('ref_axis',(1.,0.,0.));
#6697=DIRECTION('center_axis',(0.,-1.,0.));
#6698=DIRECTION('ref_axis',(1.,0.,0.));
#6699=DIRECTION('',(-0.707106781186547,0.707106781186548,-8.65956056235493E-17));
#6700=DIRECTION('center_axis',(0.,-1.,0.));
#6701=DIRECTION('ref_axis',(0.,0.,-1.));
#6702=DIRECTION('center_axis',(0.,-1.,0.));
#6703=DIRECTION('ref_axis',(1.,0.,0.));
#6704=DIRECTION('center_axis',(0.,1.,0.));
#6705=DIRECTION('ref_axis',(1.,0.,0.));
#6706=DIRECTION('center_axis',(0.,1.,0.));
#6707=DIRECTION('ref_axis',(1.,0.,0.));
#6708=DIRECTION('',(-0.447213595499958,0.894427190999916,-5.47678698264203E-17));
#6709=DIRECTION('center_axis',(0.,-1.,0.));
#6710=DIRECTION('ref_axis',(1.,0.,0.));
#6711=DIRECTION('center_axis',(0.,1.,0.));
#6712=DIRECTION('ref_axis',(1.,0.,0.));
#6713=DIRECTION('',(0.,1.,0.));
#6714=DIRECTION('center_axis',(0.,1.,0.));
#6715=DIRECTION('ref_axis',(1.,0.,0.));
#6716=DIRECTION('center_axis',(0.,-1.,0.));
#6717=DIRECTION('ref_axis',(1.,0.,0.));
#6718=DIRECTION('',(-0.707106781186547,0.707106781186548,-8.65956056235493E-17));
#6719=DIRECTION('center_axis',(0.,-1.,0.));
#6720=DIRECTION('ref_axis',(0.,0.,-1.));
#6721=DIRECTION('center_axis',(0.866025403784439,0.,-0.5));
#6722=DIRECTION('ref_axis',(0.5,0.,0.866025403784439));
#6723=DIRECTION('',(-0.5,0.,-0.866025403784439));
#6724=DIRECTION('',(0.,-1.,0.));
#6725=DIRECTION('',(0.5,0.,0.866025403784439));
#6726=DIRECTION('',(0.,-1.,0.));
#6727=DIRECTION('center_axis',(1.92296268638356E-16,0.,-1.));
#6728=DIRECTION('ref_axis',(1.,0.,1.92296268638356E-16));
#6729=DIRECTION('',(-1.,0.,-1.92296268638356E-16));
#6730=DIRECTION('',(0.,-1.,0.));
#6731=DIRECTION('',(1.,0.,1.92296268638356E-16));
#6732=DIRECTION('center_axis',(-0.866025403784439,0.,-0.5));
#6733=DIRECTION('ref_axis',(0.5,0.,-0.866025403784439));
#6734=DIRECTION('',(-0.5,0.,0.866025403784438));
#6735=DIRECTION('',(0.,-1.,0.));
#6736=DIRECTION('',(0.5,0.,-0.866025403784438));
#6737=DIRECTION('center_axis',(-0.866025403784439,0.,0.5));
#6738=DIRECTION('ref_axis',(-0.5,0.,-0.866025403784439));
#6739=DIRECTION('',(0.5,0.,0.866025403784439));
#6740=DIRECTION('',(0.,-1.,0.));
#6741=DIRECTION('',(-0.5,0.,-0.866025403784439));
#6742=DIRECTION('center_axis',(-1.92296268638356E-16,0.,1.));
#6743=DIRECTION('ref_axis',(-1.,0.,-1.92296268638356E-16));
#6744=DIRECTION('',(1.,0.,1.92296268638356E-16));
#6745=DIRECTION('',(0.,-1.,0.));
#6746=DIRECTION('',(-1.,0.,-1.92296268638356E-16));
#6747=DIRECTION('center_axis',(0.866025403784439,0.,0.5));
#6748=DIRECTION('ref_axis',(-0.5,0.,0.866025403784439));
#6749=DIRECTION('',(0.5,0.,-0.866025403784439));
#6750=DIRECTION('',(-0.5,0.,0.866025403784439));
#6751=DIRECTION('center_axis',(0.,1.,0.));
#6752=DIRECTION('ref_axis',(1.,0.,0.));
#6753=DIRECTION('center_axis',(0.,-1.,0.));
#6754=DIRECTION('ref_axis',(0.,0.,-1.));
#8614=CARTESIAN_POINT('',(0.,0.,0.));
#8615=CARTESIAN_POINT('Origin',(0.45,0.6,0.));
#8616=CARTESIAN_POINT('',(-0.45,0.6,-5.51091059616309E-17));
#8617=CARTESIAN_POINT('Origin',(0.,0.6,0.));
#8618=CARTESIAN_POINT('Origin',(0.,0.575,0.));
#8619=CARTESIAN_POINT('',(-0.5,0.55,-6.12323399573677E-17));
#8620=CARTESIAN_POINT('Origin',(0.,0.55,0.));
#8621=CARTESIAN_POINT('',(-0.475,0.575,-5.81707229594993E-17));
#8622=CARTESIAN_POINT('Origin',(0.,0.29,0.));
#8623=CARTESIAN_POINT('',(-0.5,0.0299999999999998,-6.12323399573677E-17));
#8624=CARTESIAN_POINT('Origin',(0.,0.0299999999999998,0.));
#8625=CARTESIAN_POINT('',(-0.5,0.29,-6.12323399573677E-17));
#8626=CARTESIAN_POINT('Origin',(0.,0.0150000000000001,0.));
#8627=CARTESIAN_POINT('',(-0.47,7.11236625150491E-17,-5.75583995599256E-17));
#8628=CARTESIAN_POINT('Origin',(0.,0.,0.));
#8629=CARTESIAN_POINT('',(-0.485,0.0150000000000001,-5.93953697586466E-17));
#8630=CARTESIAN_POINT('Origin',(0.32,0.,0.));
#8631=CARTESIAN_POINT('',(-0.32,-6.93889390390723E-18,-3.91886975727153E-17));
#8632=CARTESIAN_POINT('Origin',(0.,0.,0.));
#8633=CARTESIAN_POINT('Origin',(0.,-0.02,0.));
#8634=CARTESIAN_POINT('',(-0.2942,-0.0515999999999999,3.60291088309151E-17));
#8635=CARTESIAN_POINT('Origin',(0.,-0.0515999999999999,0.));
#8636=CARTESIAN_POINT('',(-0.31,-0.02,-3.7964050773568E-17));
#8637=CARTESIAN_POINT('Origin',(0.,-1.24,0.));
#8638=CARTESIAN_POINT('',(-0.2942,-2.4458,3.60291088309151E-17));
#8639=CARTESIAN_POINT('Origin',(0.,-2.4458,0.));
#8640=CARTESIAN_POINT('',(-0.2942,-1.24,-3.60291088309151E-17));
#8641=CARTESIAN_POINT('Origin',(0.,-2.47,0.));
#8642=CARTESIAN_POINT('',(-0.24,-2.5,-2.93915231795365E-17));
#8643=CARTESIAN_POINT('Origin',(0.,-2.5,0.));
#8644=CARTESIAN_POINT('',(-0.27,-2.47,-3.30654635769785E-17));
#8645=CARTESIAN_POINT('Origin',(0.,-2.5,0.));
#8646=CARTESIAN_POINT('Origin',(0.144337567297406,-0.6,-0.25));
#8647=CARTESIAN_POINT('',(0.288675134594813,-0.6,0.));
#8648=CARTESIAN_POINT('',(0.144337567297406,-0.6,-0.25));
#8649=CARTESIAN_POINT('',(0.288675134594813,-0.6,0.));
#8650=CARTESIAN_POINT('',(0.144337567297406,-0.96,-0.25));
#8651=CARTESIAN_POINT('',(0.144337567297406,-0.6,-0.25));
#8652=CARTESIAN_POINT('',(0.288675134594813,-0.96,0.));
#8653=CARTESIAN_POINT('',(0.288675134594813,-0.96,0.));
#8654=CARTESIAN_POINT('',(0.288675134594813,-0.6,0.));
#8655=CARTESIAN_POINT('Origin',(-0.144337567297406,-0.6,-0.25));
#8656=CARTESIAN_POINT('',(-0.144337567297406,-0.6,-0.25));
#8657=CARTESIAN_POINT('',(0.144337567297406,-0.6,-0.25));
#8658=CARTESIAN_POINT('',(-0.144337567297406,-0.96,-0.25));
#8659=CARTESIAN_POINT('',(-0.144337567297406,-0.6,-0.25));
#8660=CARTESIAN_POINT('',(0.144337567297406,-0.96,-0.25));
#8661=CARTESIAN_POINT('Origin',(-0.288675134594813,-0.6,-8.32667268468867E-17));
#8662=CARTESIAN_POINT('',(-0.288675134594813,-0.6,-3.53525079574969E-17));
#8663=CARTESIAN_POINT('',(-0.144337567297406,-0.6,-0.25));
#8664=CARTESIAN_POINT('',(-0.288675134594813,-0.96,-5.55111512312578E-17));
#8665=CARTESIAN_POINT('',(-0.288675134594813,-0.6,-3.53525079574969E-17));
#8666=CARTESIAN_POINT('',(-0.144337567297406,-0.96,-0.25));
#8667=CARTESIAN_POINT('Origin',(-0.144337567297407,-0.6,0.25));
#8668=CARTESIAN_POINT('',(-0.144337567297407,-0.6,0.25));
#8669=CARTESIAN_POINT('',(-0.288675134594813,-0.6,-3.53525079574969E-17));
#8670=CARTESIAN_POINT('',(-0.144337567297407,-0.96,0.25));
#8671=CARTESIAN_POINT('',(-0.144337567297407,-0.6,0.25));
#8672=CARTESIAN_POINT('',(-0.288675134594813,-0.96,-3.53525079574969E-17));
#8673=CARTESIAN_POINT('Origin',(0.144337567297406,-0.6,0.25));
#8674=CARTESIAN_POINT('',(0.144337567297406,-0.6,0.25));
#8675=CARTESIAN_POINT('',(-0.144337567297407,-0.6,0.25));
#8676=CARTESIAN_POINT('',(0.144337567297406,-0.96,0.25));
#8677=CARTESIAN_POINT('',(0.144337567297406,-0.6,0.25));
#8678=CARTESIAN_POINT('',(-0.144337567297407,-0.96,0.25));
#8679=CARTESIAN_POINT('Origin',(0.288675134594813,-0.6,0.));
#8680=CARTESIAN_POINT('',(0.144337567297406,-0.6,0.25));
#8681=CARTESIAN_POINT('',(0.144337567297406,-0.96,0.25));
#8682=CARTESIAN_POINT('Origin',(0.,-0.6,0.));
#8683=CARTESIAN_POINT('Origin',(0.,-0.96,0.));
#9404=UNCERTAINTY_MEASURE_WITH_UNIT(LENGTH_MEASURE(0.001),#9449,
'DISTANCE_ACCURACY_VALUE',
'Maximum model space distance between geometric entities at asserted c
onnectivities');
#9416=UNCERTAINTY_MEASURE_WITH_UNIT(LENGTH_MEASURE(0.001),#9449,
'DISTANCE_ACCURACY_VALUE',
'Maximum model space distance between geometric entities at asserted c
onnectivities');
#9436=(
GEOMETRIC_REPRESENTATION_CONTEXT(3)
GLOBAL_UNCERTAINTY_ASSIGNED_CONTEXT((#9404))
GLOBAL_UNIT_ASSIGNED_CONTEXT((#9449,#9451,#9452))
REPRESENTATION_CONTEXT('','3D')
);
#9448=(
GEOMETRIC_REPRESENTATION_CONTEXT(3)
GLOBAL_UNCERTAINTY_ASSIGNED_CONTEXT((#9416))
GLOBAL_UNIT_ASSIGNED_CONTEXT((#9449,#9451,#9452))
REPRESENTATION_CONTEXT('','3D')
);
#9449=(
LENGTH_UNIT()
NAMED_UNIT(*)
SI_UNIT(.CENTI.,.METRE.)
);
#9451=(
NAMED_UNIT(*)
PLANE_ANGLE_UNIT()
SI_UNIT($,.RADIAN.)
);
#9452=(
NAMED_UNIT(*)
SI_UNIT($,.STERADIAN.)
SOLID_ANGLE_UNIT()
);
#9472=SHAPE_DEFINITION_REPRESENTATION(#9508,#9576);
#9508=PRODUCT_DEFINITION_SHAPE('',$,#9608);
#9576=SHAPE_REPRESENTATION('',(#5561),#9436);
#9588=PRODUCT_DEFINITION_CONTEXT('part definition',#9683,'design');
#9608=PRODUCT_DEFINITION('Cap Screw - M6x25','Cap Screw - M6x25',#9639,
#9588);
#9639=PRODUCT_DEFINITION_FORMATION('',$,#9704);
#9683=APPLICATION_CONTEXT(
'Core Data for Automotive Mechanical Design Process');
#9684=PRODUCT_CONTEXT('part definition',#9683,'mechanical');
#9704=PRODUCT('Cap Screw - M6x25','Cap Screw - M6x25',
'Cap Screw - M6x25',(#9684));
#9779=COLOUR_RGB('Black',0.12,0.14,0.17);
#9780=FILL_AREA_STYLE_COLOUR('',#9779);
#9781=FILL_AREA_STYLE('',(#9780));
#9782=SURFACE_STYLE_FILL_AREA(#9781);
#9783=SURFACE_SIDE_STYLE('',(#9782));
#9784=SURFACE_STYLE_USAGE(.BOTH.,#9783);
#9785=PRESENTATION_STYLE_ASSIGNMENT((#9784));
ENDSEC;
END-ISO-10303-21;
